ISO-10303-21;
HEADER;
/* Generated by software containing ST-Developer
 * from STEP Tools, Inc. (www.steptools.com) 
 */
/* OPTION: using custom renumber hook */

FILE_DESCRIPTION(
/* description */ ('STEP AP242 Edition 2', 'CAx-IF Rec.Pracs.---Representation and Presentation of Product Manufa
cturing Information (PMI)---4.0---2014-10-13', 'CAx-IF Rec.Pracs.---3D Tessellated Geometry---0.4---2014-09-14', '2;1', 'CAx-IF Rec.Pracs.---User Defined Attributes---1.5---2016-08-15'),
/* implementation_level */ '2;1');

FILE_NAME(
/* name */ 'Bottle_Nech_Seal.step',
/* time_stamp */ '2026-10-08T12:15:07Z',
/* author */ (''),
/* organization */ (''),
/* preprocessor_version */ 'ST-DEVELOPER v20',
/* originating_system */ 'ONSHAPE BY PTC INC, 1.221',
/* authorisation */ '  ');

FILE_SCHEMA (('AP242_MANAGED_MODEL_BASED_3D_ENGINEERING_MIM_LF { 1 0 10303 442 3 1 4 }'));
ENDSEC;

DATA;
#25=CONICAL_SURFACE('',#14292,0.00906043638285393,0.310735335419369);
#60=COLOUR_RGB('', 0.66274510, 0.83137255, 0.94901961);
#209=SHAPE_REPRESENTATION_RELATIONSHIP('','',#13783,#236);
#236=ADVANCED_BREP_SHAPE_REPRESENTATION('',(#13727),#45473);
#591=CIRCLE('',#14278,0.0045499999999755);
#592=CIRCLE('',#14279,0.0080000000000245);
#593=CIRCLE('',#14281,0.0140000000000245);
#594=CIRCLE('',#14282,0.0045499999999755);
#595=CIRCLE('',#14284,0.0120000000000245);
#596=CIRCLE('',#14285,0.0140000000000245);
#597=CIRCLE('',#14287,0.0100000000000245);
#598=CIRCLE('',#14288,0.0120000000000245);
#599=CIRCLE('',#14290,0.0080000000000245);
#600=CIRCLE('',#14291,0.00906043638285393);
#601=CIRCLE('',#14293,0.0100000000000245);
#1273=PLANE('',#14277);
#1274=PLANE('',#14280);
#1275=PLANE('',#14283);
#1276=PLANE('',#14286);
#1277=PLANE('',#14289);
#1619=CYLINDRICAL_SURFACE('',#14294,0.0100000000000245);
#1620=CYLINDRICAL_SURFACE('',#14295,0.0120000000000245);
#1621=CYLINDRICAL_SURFACE('',#14296,0.0140000000000245);
#1622=CYLINDRICAL_SURFACE('',#14297,0.0045499999999755);
#1623=CYLINDRICAL_SURFACE('',#14298,0.0080000000000245);
#2888=ORIENTED_EDGE('',*,*,#6091,.F.);
#2889=ORIENTED_EDGE('',*,*,#6092,.T.);
#2890=ORIENTED_EDGE('',*,*,#6093,.F.);
#2891=ORIENTED_EDGE('',*,*,#6094,.T.);
#2892=ORIENTED_EDGE('',*,*,#6095,.F.);
#2893=ORIENTED_EDGE('',*,*,#6096,.T.);
#2894=ORIENTED_EDGE('',*,*,#6097,.F.);
#2895=ORIENTED_EDGE('',*,*,#6098,.T.);
#2896=ORIENTED_EDGE('',*,*,#6099,.F.);
#2897=ORIENTED_EDGE('',*,*,#6100,.T.);
#2898=ORIENTED_EDGE('',*,*,#6101,.T.);
#2899=ORIENTED_EDGE('',*,*,#6100,.F.);
#2900=ORIENTED_EDGE('',*,*,#6101,.F.);
#2901=ORIENTED_EDGE('',*,*,#6097,.T.);
#2902=ORIENTED_EDGE('',*,*,#6095,.T.);
#2903=ORIENTED_EDGE('',*,*,#6098,.F.);
#2904=ORIENTED_EDGE('',*,*,#6096,.F.);
#2905=ORIENTED_EDGE('',*,*,#6093,.T.);
#2906=ORIENTED_EDGE('',*,*,#6091,.T.);
#2907=ORIENTED_EDGE('',*,*,#6094,.F.);
#2908=ORIENTED_EDGE('',*,*,#6099,.T.);
#2909=ORIENTED_EDGE('',*,*,#6092,.F.);
#6091=EDGE_CURVE('',#7793,#7793,#591,.T.);
#6092=EDGE_CURVE('',#7794,#7794,#592,.T.);
#6093=EDGE_CURVE('',#7795,#7795,#593,.T.);
#6094=EDGE_CURVE('',#7796,#7796,#594,.T.);
#6095=EDGE_CURVE('',#7797,#7797,#595,.T.);
#6096=EDGE_CURVE('',#7798,#7798,#596,.T.);
#6097=EDGE_CURVE('',#7799,#7799,#597,.T.);
#6098=EDGE_CURVE('',#7800,#7800,#598,.T.);
#6099=EDGE_CURVE('',#7801,#7801,#599,.T.);
#6100=EDGE_CURVE('',#7802,#7802,#600,.T.);
#6101=EDGE_CURVE('',#7803,#7803,#601,.T.);
#7793=VERTEX_POINT('',#31690);
#7794=VERTEX_POINT('',#31692);
#7795=VERTEX_POINT('',#31695);
#7796=VERTEX_POINT('',#31697);
#7797=VERTEX_POINT('',#31700);
#7798=VERTEX_POINT('',#31702);
#7799=VERTEX_POINT('',#31705);
#7800=VERTEX_POINT('',#31707);
#7801=VERTEX_POINT('',#31710);
#7802=VERTEX_POINT('',#31712);
#7803=VERTEX_POINT('',#31715);
#10789=EDGE_LOOP('',(#2888));
#10790=EDGE_LOOP('',(#2889));
#10791=EDGE_LOOP('',(#2890));
#10792=EDGE_LOOP('',(#2891));
#10793=EDGE_LOOP('',(#2892));
#10794=EDGE_LOOP('',(#2893));
#10795=EDGE_LOOP('',(#2894));
#10796=EDGE_LOOP('',(#2895));
#10797=EDGE_LOOP('',(#2896));
#10798=EDGE_LOOP('',(#2897));
#10799=EDGE_LOOP('',(#2898));
#10800=EDGE_LOOP('',(#2899));
#10801=EDGE_LOOP('',(#2900));
#10802=EDGE_LOOP('',(#2901));
#10803=EDGE_LOOP('',(#2902));
#10804=EDGE_LOOP('',(#2903));
#10805=EDGE_LOOP('',(#2904));
#10806=EDGE_LOOP('',(#2905));
#10807=EDGE_LOOP('',(#2906));
#10808=EDGE_LOOP('',(#2907));
#10809=EDGE_LOOP('',(#2908));
#10810=EDGE_LOOP('',(#2909));
#11906=FACE_BOUND('',#10789,.T.);
#11907=FACE_BOUND('',#10790,.T.);
#11908=FACE_BOUND('',#10791,.T.);
#11909=FACE_BOUND('',#10792,.T.);
#11910=FACE_BOUND('',#10793,.T.);
#11911=FACE_BOUND('',#10794,.T.);
#11912=FACE_BOUND('',#10795,.T.);
#11913=FACE_BOUND('',#10796,.T.);
#11914=FACE_BOUND('',#10797,.T.);
#11915=FACE_BOUND('',#10798,.T.);
#11916=FACE_BOUND('',#10799,.T.);
#11917=FACE_BOUND('',#10800,.T.);
#11918=FACE_BOUND('',#10801,.T.);
#11919=FACE_BOUND('',#10802,.T.);
#11920=FACE_BOUND('',#10803,.T.);
#11921=FACE_BOUND('',#10804,.T.);
#11922=FACE_BOUND('',#10805,.T.);
#11923=FACE_BOUND('',#10806,.T.);
#11924=FACE_BOUND('',#10807,.T.);
#11925=FACE_BOUND('',#10808,.T.);
#11926=FACE_BOUND('',#10809,.T.);
#11927=FACE_BOUND('',#10810,.T.);
#12943=ADVANCED_FACE('',(#11906,#11907),#1273,.T.);
#12944=ADVANCED_FACE('',(#11908,#11909),#1274,.T.);
#12945=ADVANCED_FACE('',(#11910,#11911),#1275,.T.);
#12946=ADVANCED_FACE('',(#11912,#11913),#1276,.T.);
#12947=ADVANCED_FACE('',(#11914,#11915),#1277,.T.);
#12948=ADVANCED_FACE('',(#11916,#11917),#25,.T.);
#12949=ADVANCED_FACE('',(#11918,#11919),#1619,.T.);
#12950=ADVANCED_FACE('',(#11920,#11921),#1620,.F.);
#12951=ADVANCED_FACE('',(#11922,#11923),#1621,.T.);
#12952=ADVANCED_FACE('',(#11924,#11925),#1622,.F.);
#12953=ADVANCED_FACE('',(#11926,#11927),#1623,.F.);
#13510=CLOSED_SHELL('',(#12943,#12944,#12945,#12946,#12947,#12948,#12949,
#12950,#12951,#12952,#12953));
#13537=STYLED_ITEM('',(#13564),#13727);
#13564=PRESENTATION_STYLE_ASSIGNMENT((#13591));
#13591=SURFACE_STYLE_USAGE(.BOTH.,#13618);
#13618=SURFACE_SIDE_STYLE('',(#13645));
#13645=SURFACE_STYLE_FILL_AREA(#13672);
#13672=FILL_AREA_STYLE('',(#13699));
#13699=FILL_AREA_STYLE_COLOUR('',#60);
#13727=MANIFOLD_SOLID_BREP('Bottle_Nech_Seal',#13510);
#13755=SHAPE_DEFINITION_REPRESENTATION(#45542,#13783);
#13783=SHAPE_REPRESENTATION('Bottle_Nech_Seal',(#13802),#45473);
#13802=AXIS2_PLACEMENT_3D('',#19109,#15295,#15296);
#14277=AXIS2_PLACEMENT_3D('',#31688,#16364,#16365);
#14278=AXIS2_PLACEMENT_3D('',#31689,#16366,#16367);
#14279=AXIS2_PLACEMENT_3D('',#31691,#16368,#16369);
#14280=AXIS2_PLACEMENT_3D('',#31693,#16370,#16371);
#14281=AXIS2_PLACEMENT_3D('',#31694,#16372,#16373);
#14282=AXIS2_PLACEMENT_3D('',#31696,#16374,#16375);
#14283=AXIS2_PLACEMENT_3D('',#31698,#16376,#16377);
#14284=AXIS2_PLACEMENT_3D('',#31699,#16378,#16379);
#14285=AXIS2_PLACEMENT_3D('',#31701,#16380,#16381);
#14286=AXIS2_PLACEMENT_3D('',#31703,#16382,#16383);
#14287=AXIS2_PLACEMENT_3D('',#31704,#16384,#16385);
#14288=AXIS2_PLACEMENT_3D('',#31706,#16386,#16387);
#14289=AXIS2_PLACEMENT_3D('',#31708,#16388,#16389);
#14290=AXIS2_PLACEMENT_3D('',#31709,#16390,#16391);
#14291=AXIS2_PLACEMENT_3D('',#31711,#16392,#16393);
#14292=AXIS2_PLACEMENT_3D('',#31713,#16394,#16395);
#14293=AXIS2_PLACEMENT_3D('',#31714,#16396,#16397);
#14294=AXIS2_PLACEMENT_3D('',#31716,#16398,#16399);
#14295=AXIS2_PLACEMENT_3D('',#31717,#16400,#16401);
#14296=AXIS2_PLACEMENT_3D('',#31718,#16402,#16403);
#14297=AXIS2_PLACEMENT_3D('',#31719,#16404,#16405);
#14298=AXIS2_PLACEMENT_3D('',#31720,#16406,#16407);
#15295=DIRECTION('',(0.,0.,1.));
#15296=DIRECTION('',(1.,0.,0.));
#16364=DIRECTION('',(0.,0.,-1.));
#16365=DIRECTION('',(-1.,0.,0.));
#16366=DIRECTION('',(0.,0.,-1.));
#16367=DIRECTION('',(-1.,0.,0.));
#16368=DIRECTION('',(0.,0.,-1.));
#16369=DIRECTION('',(-1.,0.,0.));
#16370=DIRECTION('',(0.,0.,1.));
#16371=DIRECTION('',(1.,0.,0.));
#16372=DIRECTION('',(0.,0.,-1.));
#16373=DIRECTION('',(-1.,0.,0.));
#16374=DIRECTION('',(0.,0.,-1.));
#16375=DIRECTION('',(-1.,0.,0.));
#16376=DIRECTION('',(0.,0.,-1.));
#16377=DIRECTION('',(-1.,0.,0.));
#16378=DIRECTION('',(0.,0.,-1.));
#16379=DIRECTION('',(-1.,0.,0.));
#16380=DIRECTION('',(0.,0.,-1.));
#16381=DIRECTION('',(-1.,0.,0.));
#16382=DIRECTION('',(0.,0.,-1.));
#16383=DIRECTION('',(-1.,0.,0.));
#16384=DIRECTION('',(0.,0.,-1.));
#16385=DIRECTION('',(-1.,0.,0.));
#16386=DIRECTION('',(0.,0.,-1.));
#16387=DIRECTION('',(-1.,0.,0.));
#16388=DIRECTION('',(0.,0.,-1.));
#16389=DIRECTION('',(-1.,0.,0.));
#16390=DIRECTION('',(0.,0.,-1.));
#16391=DIRECTION('',(-1.,0.,0.));
#16392=DIRECTION('',(0.,0.,-1.));
#16393=DIRECTION('',(-1.,0.,0.));
#16394=DIRECTION('',(0.,0.,1.));
#16395=DIRECTION('',(1.,0.,0.));
#16396=DIRECTION('',(0.,0.,-1.));
#16397=DIRECTION('',(-1.,0.,0.));
#16398=DIRECTION('',(0.,0.,-1.));
#16399=DIRECTION('',(-1.,0.,0.));
#16400=DIRECTION('',(0.,0.,-1.));
#16401=DIRECTION('',(-1.,0.,0.));
#16402=DIRECTION('',(0.,0.,-1.));
#16403=DIRECTION('',(-1.,0.,0.));
#16404=DIRECTION('',(0.,0.,-1.));
#16405=DIRECTION('',(-1.,0.,0.));
#16406=DIRECTION('',(0.,0.,-1.));
#16407=DIRECTION('',(-1.,0.,0.));
#19109=CARTESIAN_POINT('',(0.,0.,0.));
#31688=CARTESIAN_POINT('',(0.,0.0100000000000245,0.054000001));
#31689=CARTESIAN_POINT('',(0.,0.,0.054000001));
#31690=CARTESIAN_POINT('',(-0.0045499999999755,0.,0.054000001));
#31691=CARTESIAN_POINT('',(0.,0.,0.054000001));
#31692=CARTESIAN_POINT('',(-0.0080000000000245,0.,0.054000001));
#31693=CARTESIAN_POINT('',(0.,0.0140000000000245,0.056000001));
#31694=CARTESIAN_POINT('',(0.,0.,0.056000001));
#31695=CARTESIAN_POINT('',(-0.0140000000000245,0.,0.056000001));
#31696=CARTESIAN_POINT('',(0.,0.,0.056000001));
#31697=CARTESIAN_POINT('',(-0.0045499999999755,0.,0.056000001));
#31698=CARTESIAN_POINT('',(0.,0.0120000000000245,0.050900001));
#31699=CARTESIAN_POINT('',(0.,0.,0.050900001));
#31700=CARTESIAN_POINT('',(-0.0120000000000245,0.,0.050900001));
#31701=CARTESIAN_POINT('',(0.,0.,0.050900001));
#31702=CARTESIAN_POINT('',(-0.0140000000000245,0.,0.050900001));
#31703=CARTESIAN_POINT('',(0.,0.0100000000000245,0.054000001));
#31704=CARTESIAN_POINT('',(0.,0.,0.054000001));
#31705=CARTESIAN_POINT('',(-0.0100000000000245,0.,0.054000001));
#31706=CARTESIAN_POINT('',(0.,0.,0.054000001));
#31707=CARTESIAN_POINT('',(-0.0120000000000245,0.,0.054000001));
#31708=CARTESIAN_POINT('',(0.,0.0080000000000245,0.04185765489));
#31709=CARTESIAN_POINT('',(0.,0.,0.04185765489));
#31710=CARTESIAN_POINT('',(-0.0080000000000245,0.,0.04185765489));
#31711=CARTESIAN_POINT('',(0.,0.,0.04185765489));
#31712=CARTESIAN_POINT('',(-0.00906043638285393,0.,0.04185765489));
#31713=CARTESIAN_POINT('',(0.,0.,0.04185765489));
#31714=CARTESIAN_POINT('',(0.,0.,0.0447833821488957));
#31715=CARTESIAN_POINT('',(-0.0100000000000245,0.,0.0447833821488957));
#31716=CARTESIAN_POINT('',(0.,0.,0.));
#31717=CARTESIAN_POINT('',(0.,0.,0.));
#31718=CARTESIAN_POINT('',(0.,0.,0.));
#31719=CARTESIAN_POINT('',(0.,0.,0.));
#31720=CARTESIAN_POINT('',(0.,0.,0.));
#45463=MECHANICAL_DESIGN_GEOMETRIC_PRESENTATION_REPRESENTATION('',(#13537),#45464);
#45464=(
GEOMETRIC_REPRESENTATION_CONTEXT(3)
GLOBAL_UNCERTAINTY_ASSIGNED_CONTEXT((#45492))
GLOBAL_UNIT_ASSIGNED_CONTEXT((#45522,#45521,#45520))
REPRESENTATION_CONTEXT('MAS-690','TOP_LEVEL_ASSEMBLY_PART')
);
#45473=(
GEOMETRIC_REPRESENTATION_CONTEXT(3)
GLOBAL_UNCERTAINTY_ASSIGNED_CONTEXT((#45501))
GLOBAL_UNIT_ASSIGNED_CONTEXT((#45522,#45521,#45520))
REPRESENTATION_CONTEXT('Bottle_Nech_Seal','COMPONENT_PART')
);
#45492=UNCERTAINTY_MEASURE_WITH_UNIT(LENGTH_MEASURE(1.E-8),#45522,
'DISTANCE_ACCURACY_VALUE','Maximum Tolerance applied to model');
#45501=UNCERTAINTY_MEASURE_WITH_UNIT(LENGTH_MEASURE(1.E-8),#45522,
'DISTANCE_ACCURACY_VALUE','Maximum Tolerance applied to model');
#45520=(
NAMED_UNIT(*)
SI_UNIT($,.STERADIAN.)
SOLID_ANGLE_UNIT()
);
#45521=(
NAMED_UNIT(*)
PLANE_ANGLE_UNIT()
SI_UNIT($,.RADIAN.)
);
#45522=(
LENGTH_UNIT()
NAMED_UNIT(*)
SI_UNIT($,.METRE.)
);
#45542=PRODUCT_DEFINITION_SHAPE('','',#45594);
#45594=PRODUCT_DEFINITION('','',#45650,#45622);
#45622=PRODUCT_DEFINITION_CONTEXT('',#45782,'design');
#45650=PRODUCT_DEFINITION_FORMATION_WITH_SPECIFIED_SOURCE('','',#45706,
 .NOT_KNOWN.);
#45706=PRODUCT('Bottle_Nech_Seal','Bottle_Nech_Seal','Bottle_Nech_Seal',
(#45762));
#45762=PRODUCT_CONTEXT('',#45782,'mechanical');
#45782=APPLICATION_CONTEXT('managed model based 3d engineering');
ENDSEC;
END-ISO-10303-21;
